ISO-10303-21;
HEADER;
/* Generated by software containing ST-Developer
 * from STEP Tools, Inc. (www.steptools.com) 
 */

FILE_DESCRIPTION(
/* description */ ('PAT-026'),
/* implementation_level */ '2;1');

FILE_NAME(
/* name */ 'Plain shaft (1).step',
/* time_stamp */ '2026-10-28T22:25:58-07:00',
/* author */ (''),
/* organization */ (''),
/* preprocessor_version */ 'ST-DEVELOPER v20.2',
/* originating_system */ 'Autodesk Translation Framework v15.17.0.0',
/* authorisation */ '');

FILE_SCHEMA (('AUTOMOTIVE_DESIGN { 1 0 10303 214 3 1 1 }'));
ENDSEC;

DATA;
#10=MECHANICAL_DESIGN_GEOMETRIC_PRESENTATION_REPRESENTATION('',(#143),#12343);
#121=SHAPE_REPRESENTATION_RELATIONSHIP('SRR','None',#12398,#132);
#132=ADVANCED_BREP_SHAPE_REPRESENTATION('',(#154),#12333);
#143=STYLED_ITEM('',(#12533),#154);
#154=MANIFOLD_SOLID_BREP('Body1',#7349);
#202=PLANE('',#7512);
#203=PLANE('',#7513);
#566=FACE_OUTER_BOUND('',#977,.T.);
#567=FACE_OUTER_BOUND('',#978,.T.);
#568=FACE_OUTER_BOUND('',#979,.T.);
#977=EDGE_LOOP('',(#4953,#4954,#4955,#4956));
#978=EDGE_LOOP('',(#4957));
#979=EDGE_LOOP('',(#4958));
#1409=LINE('',#10106,#2281);
#2281=VECTOR('',#8119,0.6);
#3146=CIRCLE('',#7510,0.6);
#3147=CIRCLE('',#7511,0.6);
#3279=VERTEX_POINT('',#10103);
#3280=VERTEX_POINT('',#10105);
#3920=EDGE_CURVE('',#3279,#3279,#3146,.T.);
#3921=EDGE_CURVE('',#3279,#3280,#1409,.T.);
#3922=EDGE_CURVE('',#3280,#3280,#3147,.T.);
#4953=ORIENTED_EDGE('',*,*,#3920,.F.);
#4954=ORIENTED_EDGE('',*,*,#3921,.T.);
#4955=ORIENTED_EDGE('',*,*,#3922,.T.);
#4956=ORIENTED_EDGE('',*,*,#3921,.F.);
#4957=ORIENTED_EDGE('',*,*,#3920,.T.);
#4958=ORIENTED_EDGE('',*,*,#3922,.F.);
#6916=CYLINDRICAL_SURFACE('',#7509,0.6);
#6957=ADVANCED_FACE('',(#566),#6916,.T.);
#6958=ADVANCED_FACE('',(#567),#202,.T.);
#6959=ADVANCED_FACE('',(#568),#203,.F.);
#7349=CLOSED_SHELL('',(#6957,#6958,#6959));
#7508=AXIS2_PLACEMENT_3D('',#10101,#8113,#8114);
#7509=AXIS2_PLACEMENT_3D('',#10102,#8115,#8116);
#7510=AXIS2_PLACEMENT_3D('',#10104,#8117,#8118);
#7511=AXIS2_PLACEMENT_3D('',#10107,#8120,#8121);
#7512=AXIS2_PLACEMENT_3D('',#10108,#8122,#8123);
#7513=AXIS2_PLACEMENT_3D('',#10109,#8124,#8125);
#8113=DIRECTION('axis',(0.,0.,1.));
#8114=DIRECTION('refdir',(1.,0.,0.));
#8115=DIRECTION('center_axis',(0.,1.,0.));
#8116=DIRECTION('ref_axis',(1.,0.,0.));
#8117=DIRECTION('center_axis',(0.,1.,0.));
#8118=DIRECTION('ref_axis',(1.,0.,0.));
#8119=DIRECTION('',(0.,-1.,0.));
#8120=DIRECTION('center_axis',(0.,1.,0.));
#8121=DIRECTION('ref_axis',(1.,0.,0.));
#8122=DIRECTION('center_axis',(0.,1.,0.));
#8123=DIRECTION('ref_axis',(1.,0.,0.));
#8124=DIRECTION('center_axis',(0.,1.,0.));
#8125=DIRECTION('ref_axis',(1.,0.,0.));
#10101=CARTESIAN_POINT('',(0.,0.,0.));
#10102=CARTESIAN_POINT('Origin',(0.,0.4,3.5));
#10103=CARTESIAN_POINT('',(-0.6,13.,3.5));
#10104=CARTESIAN_POINT('Origin',(0.,13.,3.5));
#10105=CARTESIAN_POINT('',(-0.6,0.4,3.5));
#10106=CARTESIAN_POINT('',(-0.6,0.4,3.5));
#10107=CARTESIAN_POINT('Origin',(0.,0.4,3.5));
#10108=CARTESIAN_POINT('Origin',(0.,13.,3.5));
#10109=CARTESIAN_POINT('Origin',(0.,0.4,3.5));
#12319=UNCERTAINTY_MEASURE_WITH_UNIT(LENGTH_MEASURE(0.001),#12344,
'DISTANCE_ACCURACY_VALUE',
'Maximum model space distance between geometric entities at asserted c
onnectivities');
#12329=UNCERTAINTY_MEASURE_WITH_UNIT(LENGTH_MEASURE(0.001),#12344,
'DISTANCE_ACCURACY_VALUE',
'Maximum model space distance between geometric entities at asserted c
onnectivities');
#12333=(
GEOMETRIC_REPRESENTATION_CONTEXT(3)
GLOBAL_UNCERTAINTY_ASSIGNED_CONTEXT((#12319))
GLOBAL_UNIT_ASSIGNED_CONTEXT((#12344,#12346,#12347))
REPRESENTATION_CONTEXT('','3D')
);
#12343=(
GEOMETRIC_REPRESENTATION_CONTEXT(3)
GLOBAL_UNCERTAINTY_ASSIGNED_CONTEXT((#12329))
GLOBAL_UNIT_ASSIGNED_CONTEXT((#12344,#12346,#12347))
REPRESENTATION_CONTEXT('','3D')
);
#12344=(
LENGTH_UNIT()
NAMED_UNIT(*)
SI_UNIT(.CENTI.,.METRE.)
);
#12346=(
NAMED_UNIT(*)
PLANE_ANGLE_UNIT()
SI_UNIT($,.RADIAN.)
);
#12347=(
NAMED_UNIT(*)
SI_UNIT($,.STERADIAN.)
SOLID_ANGLE_UNIT()
);
#12351=SHAPE_DEFINITION_REPRESENTATION(#12364,#12398);
#12364=PRODUCT_DEFINITION_SHAPE('',$,#12412);
#12398=SHAPE_REPRESENTATION('',(#7508),#12333);
#12408=PRODUCT_DEFINITION_CONTEXT('part definition',#12449,'design');
#12412=PRODUCT_DEFINITION('Plain shaft (1)','Plain shaft (1)',
#12425,#12408);
#12425=PRODUCT_DEFINITION_FORMATION('',$,#12454);
#12449=APPLICATION_CONTEXT(
'Core Data for Automotive Mechanical Design Process');
#12450=PRODUCT_CONTEXT('part definition',#12449,'mechanical');
#12454=PRODUCT('Plain shaft (1)','Plain shaft (1)',
'Plain shaft (1)',(#12450));
#12527=COLOUR_RGB('Grey',0.48,0.52,0.57);
#12528=FILL_AREA_STYLE_COLOUR('',#12527);
#12529=FILL_AREA_STYLE('',(#12528));
#12530=SURFACE_STYLE_FILL_AREA(#12529);
#12531=SURFACE_SIDE_STYLE('',(#12530));
#12532=SURFACE_STYLE_USAGE(.BOTH.,#12531);
#12533=PRESENTATION_STYLE_ASSIGNMENT((#12532));
ENDSEC;
END-ISO-10303-21;
